ISO-10303-21;
HEADER;
/* Generated by software containing ST-Developer
 * from STEP Tools, Inc. (www.steptools.com) 
 */

FILE_DESCRIPTION(
/* description */ (''),
/* implementation_level */ '2;1');

FILE_NAME(
/* name */ 'Screw_02.step',
/* time_stamp */ '2026-10-05T21:34:53-07:00',
/* author */ (''),
/* organization */ (''),
/* preprocessor_version */ 'ST-DEVELOPER v20.2',
/* originating_system */ 'Autodesk Translation Framework v15.15.0.0',
/* authorisation */ '');

FILE_SCHEMA (('AUTOMOTIVE_DESIGN { 1 0 10303 214 3 1 1 }'));
ENDSEC;

DATA;
#10=MECHANICAL_DESIGN_GEOMETRIC_PRESENTATION_REPRESENTATION('',(#69),#9822);
#51=SHAPE_REPRESENTATION_RELATIONSHIP('SRR','None',#9861,#60);
#60=ADVANCED_BREP_SHAPE_REPRESENTATION('',(#78),#9817);
#69=STYLED_ITEM('',(#9912),#78);
#78=MANIFOLD_SOLID_BREP('Body1',#3292);
#96=FACE_BOUND('',#619,.T.);
#238=PLANE('',#3658);
#239=PLANE('',#3659);
#240=PLANE('',#3660);
#241=PLANE('',#3661);
#242=PLANE('',#3662);
#243=PLANE('',#3663);
#244=PLANE('',#3664);
#245=PLANE('',#3668);
#246=PLANE('',#3669);
#412=FACE_OUTER_BOUND('',#610,.T.);
#413=FACE_OUTER_BOUND('',#611,.T.);
#414=FACE_OUTER_BOUND('',#612,.T.);
#415=FACE_OUTER_BOUND('',#613,.T.);
#416=FACE_OUTER_BOUND('',#614,.T.);
#417=FACE_OUTER_BOUND('',#615,.T.);
#418=FACE_OUTER_BOUND('',#616,.T.);
#419=FACE_OUTER_BOUND('',#617,.T.);
#420=FACE_OUTER_BOUND('',#618,.T.);
#421=FACE_OUTER_BOUND('',#620,.T.);
#610=EDGE_LOOP('',(#2876,#2877,#2878,#2879));
#611=EDGE_LOOP('',(#2880,#2881,#2882,#2883));
#612=EDGE_LOOP('',(#2884,#2885,#2886,#2887));
#613=EDGE_LOOP('',(#2888,#2889,#2890,#2891));
#614=EDGE_LOOP('',(#2892,#2893,#2894,#2895));
#615=EDGE_LOOP('',(#2896,#2897,#2898,#2899));
#616=EDGE_LOOP('',(#2900,#2901,#2902,#2903,#2904,#2905));
#617=EDGE_LOOP('',(#2906,#2907,#2908,#2909));
#618=EDGE_LOOP('',(#2910));
#619=EDGE_LOOP('',(#2911,#2912,#2913,#2914,#2915,#2916));
#620=EDGE_LOOP('',(#2917));
#857=LINE('',#9560,#1116);
#858=LINE('',#9562,#1117);
#859=LINE('',#9564,#1118);
#860=LINE('',#9565,#1119);
#861=LINE('',#9568,#1120);
#862=LINE('',#9570,#1121);
#863=LINE('',#9571,#1122);
#864=LINE('',#9574,#1123);
#865=LINE('',#9576,#1124);
#866=LINE('',#9577,#1125);
#867=LINE('',#9580,#1126);
#868=LINE('',#9582,#1127);
#869=LINE('',#9583,#1128);
#870=LINE('',#9586,#1129);
#871=LINE('',#9588,#1130);
#872=LINE('',#9589,#1131);
#873=LINE('',#9591,#1132);
#874=LINE('',#9592,#1133);
#875=LINE('',#9598,#1134);
#1116=VECTOR('',#4457,10.);
#1117=VECTOR('',#4458,10.);
#1118=VECTOR('',#4459,10.);
#1119=VECTOR('',#4460,10.);
#1120=VECTOR('',#4463,10.);
#1121=VECTOR('',#4464,10.);
#1122=VECTOR('',#4465,10.);
#1123=VECTOR('',#4468,10.);
#1124=VECTOR('',#4469,10.);
#1125=VECTOR('',#4470,10.);
#1126=VECTOR('',#4473,9.99999999999999);
#1127=VECTOR('',#4474,9.99999999999999);
#1128=VECTOR('',#4475,10.);
#1129=VECTOR('',#4478,10.);
#1130=VECTOR('',#4479,10.);
#1131=VECTOR('',#4480,10.);
#1132=VECTOR('',#4483,10.);
#1133=VECTOR('',#4484,10.);
#1134=VECTOR('',#4491,1.);
#1301=CIRCLE('',#3666,1.);
#1302=CIRCLE('',#3667,1.);
#1575=VERTEX_POINT('',#9558);
#1576=VERTEX_POINT('',#9559);
#1577=VERTEX_POINT('',#9561);
#1578=VERTEX_POINT('',#9563);
#1579=VERTEX_POINT('',#9567);
#1580=VERTEX_POINT('',#9569);
#1581=VERTEX_POINT('',#9573);
#1582=VERTEX_POINT('',#9575);
#1583=VERTEX_POINT('',#9579);
#1584=VERTEX_POINT('',#9581);
#1585=VERTEX_POINT('',#9585);
#1586=VERTEX_POINT('',#9587);
#1587=VERTEX_POINT('',#9595);
#1588=VERTEX_POINT('',#9597);
#2017=EDGE_CURVE('',#1575,#1576,#857,.T.);
#2018=EDGE_CURVE('',#1576,#1577,#858,.T.);
#2019=EDGE_CURVE('',#1578,#1577,#859,.T.);
#2020=EDGE_CURVE('',#1575,#1578,#860,.T.);
#2021=EDGE_CURVE('',#1579,#1575,#861,.T.);
#2022=EDGE_CURVE('',#1580,#1578,#862,.T.);
#2023=EDGE_CURVE('',#1579,#1580,#863,.T.);
#2024=EDGE_CURVE('',#1581,#1579,#864,.T.);
#2025=EDGE_CURVE('',#1582,#1580,#865,.T.);
#2026=EDGE_CURVE('',#1581,#1582,#866,.T.);
#2027=EDGE_CURVE('',#1583,#1581,#867,.T.);
#2028=EDGE_CURVE('',#1584,#1582,#868,.T.);
#2029=EDGE_CURVE('',#1583,#1584,#869,.T.);
#2030=EDGE_CURVE('',#1585,#1583,#870,.T.);
#2031=EDGE_CURVE('',#1586,#1584,#871,.T.);
#2032=EDGE_CURVE('',#1585,#1586,#872,.T.);
#2033=EDGE_CURVE('',#1576,#1585,#873,.T.);
#2034=EDGE_CURVE('',#1577,#1586,#874,.T.);
#2035=EDGE_CURVE('',#1587,#1587,#1301,.T.);
#2036=EDGE_CURVE('',#1587,#1588,#875,.T.);
#2037=EDGE_CURVE('',#1588,#1588,#1302,.T.);
#2876=ORIENTED_EDGE('',*,*,#2017,.T.);
#2877=ORIENTED_EDGE('',*,*,#2018,.T.);
#2878=ORIENTED_EDGE('',*,*,#2019,.F.);
#2879=ORIENTED_EDGE('',*,*,#2020,.F.);
#2880=ORIENTED_EDGE('',*,*,#2021,.T.);
#2881=ORIENTED_EDGE('',*,*,#2020,.T.);
#2882=ORIENTED_EDGE('',*,*,#2022,.F.);
#2883=ORIENTED_EDGE('',*,*,#2023,.F.);
#2884=ORIENTED_EDGE('',*,*,#2024,.T.);
#2885=ORIENTED_EDGE('',*,*,#2023,.T.);
#2886=ORIENTED_EDGE('',*,*,#2025,.F.);
#2887=ORIENTED_EDGE('',*,*,#2026,.F.);
#2888=ORIENTED_EDGE('',*,*,#2027,.T.);
#2889=ORIENTED_EDGE('',*,*,#2026,.T.);
#2890=ORIENTED_EDGE('',*,*,#2028,.F.);
#2891=ORIENTED_EDGE('',*,*,#2029,.F.);
#2892=ORIENTED_EDGE('',*,*,#2030,.T.);
#2893=ORIENTED_EDGE('',*,*,#2029,.T.);
#2894=ORIENTED_EDGE('',*,*,#2031,.F.);
#2895=ORIENTED_EDGE('',*,*,#2032,.F.);
#2896=ORIENTED_EDGE('',*,*,#2033,.T.);
#2897=ORIENTED_EDGE('',*,*,#2032,.T.);
#2898=ORIENTED_EDGE('',*,*,#2034,.F.);
#2899=ORIENTED_EDGE('',*,*,#2018,.F.);
#2900=ORIENTED_EDGE('',*,*,#2034,.T.);
#2901=ORIENTED_EDGE('',*,*,#2031,.T.);
#2902=ORIENTED_EDGE('',*,*,#2028,.T.);
#2903=ORIENTED_EDGE('',*,*,#2025,.T.);
#2904=ORIENTED_EDGE('',*,*,#2022,.T.);
#2905=ORIENTED_EDGE('',*,*,#2019,.T.);
#2906=ORIENTED_EDGE('',*,*,#2035,.F.);
#2907=ORIENTED_EDGE('',*,*,#2036,.T.);
#2908=ORIENTED_EDGE('',*,*,#2037,.T.);
#2909=ORIENTED_EDGE('',*,*,#2036,.F.);
#2910=ORIENTED_EDGE('',*,*,#2037,.F.);
#2911=ORIENTED_EDGE('',*,*,#2017,.F.);
#2912=ORIENTED_EDGE('',*,*,#2021,.F.);
#2913=ORIENTED_EDGE('',*,*,#2024,.F.);
#2914=ORIENTED_EDGE('',*,*,#2027,.F.);
#2915=ORIENTED_EDGE('',*,*,#2030,.F.);
#2916=ORIENTED_EDGE('',*,*,#2033,.F.);
#2917=ORIENTED_EDGE('',*,*,#2035,.T.);
#3092=CYLINDRICAL_SURFACE('',#3665,1.);
#3250=ADVANCED_FACE('',(#412),#238,.T.);
#3251=ADVANCED_FACE('',(#413),#239,.T.);
#3252=ADVANCED_FACE('',(#414),#240,.T.);
#3253=ADVANCED_FACE('',(#415),#241,.T.);
#3254=ADVANCED_FACE('',(#416),#242,.T.);
#3255=ADVANCED_FACE('',(#417),#243,.T.);
#3256=ADVANCED_FACE('',(#418),#244,.T.);
#3257=ADVANCED_FACE('',(#419),#3092,.T.);
#3258=ADVANCED_FACE('',(#420,#96),#245,.F.);
#3259=ADVANCED_FACE('',(#421),#246,.T.);
#3292=CLOSED_SHELL('',(#3250,#3251,#3252,#3253,#3254,#3255,#3256,#3257,
#3258,#3259));
#3657=AXIS2_PLACEMENT_3D('',#9556,#4453,#4454);
#3658=AXIS2_PLACEMENT_3D('',#9557,#4455,#4456);
#3659=AXIS2_PLACEMENT_3D('',#9566,#4461,#4462);
#3660=AXIS2_PLACEMENT_3D('',#9572,#4466,#4467);
#3661=AXIS2_PLACEMENT_3D('',#9578,#4471,#4472);
#3662=AXIS2_PLACEMENT_3D('',#9584,#4476,#4477);
#3663=AXIS2_PLACEMENT_3D('',#9590,#4481,#4482);
#3664=AXIS2_PLACEMENT_3D('',#9593,#4485,#4486);
#3665=AXIS2_PLACEMENT_3D('',#9594,#4487,#4488);
#3666=AXIS2_PLACEMENT_3D('',#9596,#4489,#4490);
#3667=AXIS2_PLACEMENT_3D('',#9599,#4492,#4493);
#3668=AXIS2_PLACEMENT_3D('',#9600,#4494,#4495);
#3669=AXIS2_PLACEMENT_3D('',#9601,#4496,#4497);
#4453=DIRECTION('axis',(0.,0.,1.));
#4454=DIRECTION('refdir',(1.,0.,0.));
#4455=DIRECTION('center_axis',(0.855116261416916,0.,0.518436282932008));
#4456=DIRECTION('ref_axis',(0.518436282932008,0.,-0.855116261416916));
#4457=DIRECTION('',(0.518436282932008,0.,-0.855116261416916));
#4458=DIRECTION('',(0.,1.,0.));
#4459=DIRECTION('',(0.518436282932008,0.,-0.855116261416916));
#4460=DIRECTION('',(0.,1.,0.));
#4461=DIRECTION('center_axis',(0.876537121971153,0.,-0.481334264110221));
#4462=DIRECTION('ref_axis',(-0.481334264110221,0.,-0.876537121971153));
#4463=DIRECTION('',(-0.481334264110221,0.,-0.876537121971153));
#4464=DIRECTION('',(-0.481334264110221,0.,-0.876537121971153));
#4465=DIRECTION('',(0.,1.,0.));
#4466=DIRECTION('center_axis',(0.0214208605542369,0.,-0.999770547042228));
#4467=DIRECTION('ref_axis',(-0.999770547042228,0.,-0.0214208605542369));
#4468=DIRECTION('',(-0.999770547042228,0.,-0.0214208605542369));
#4469=DIRECTION('',(-0.999770547042228,0.,-0.0214208605542369));
#4470=DIRECTION('',(0.,1.,0.));
#4471=DIRECTION('center_axis',(-0.855116261416916,0.,-0.518436282932007));
#4472=DIRECTION('ref_axis',(-0.518436282932007,0.,0.855116261416916));
#4473=DIRECTION('',(-0.518436282932007,0.,0.855116261416916));
#4474=DIRECTION('',(-0.518436282932007,0.,0.855116261416916));
#4475=DIRECTION('',(0.,1.,0.));
#4476=DIRECTION('center_axis',(-0.876537121971153,0.,0.481334264110221));
#4477=DIRECTION('ref_axis',(0.481334264110221,0.,0.876537121971153));
#4478=DIRECTION('',(0.481334264110221,0.,0.876537121971153));
#4479=DIRECTION('',(0.481334264110221,0.,0.876537121971153));
#4480=DIRECTION('',(0.,1.,0.));
#4481=DIRECTION('center_axis',(-0.0214208605542369,0.,0.999770547042228));
#4482=DIRECTION('ref_axis',(0.999770547042228,0.,0.0214208605542369));
#4483=DIRECTION('',(0.999770547042228,0.,0.0214208605542369));
#4484=DIRECTION('',(0.999770547042228,0.,0.0214208605542369));
#4485=DIRECTION('center_axis',(0.,-1.,0.));
#4486=DIRECTION('ref_axis',(0.,0.,-1.));
#4487=DIRECTION('center_axis',(0.,1.,0.));
#4488=DIRECTION('ref_axis',(1.,0.,0.));
#4489=DIRECTION('center_axis',(0.,1.,0.));
#4490=DIRECTION('ref_axis',(1.,0.,0.));
#4491=DIRECTION('',(0.,-1.,0.));
#4492=DIRECTION('center_axis',(0.,1.,0.));
#4493=DIRECTION('ref_axis',(1.,0.,0.));
#4494=DIRECTION('center_axis',(0.,1.,0.));
#4495=DIRECTION('ref_axis',(1.,0.,0.));
#4496=DIRECTION('center_axis',(0.,1.,0.));
#4497=DIRECTION('ref_axis',(1.,0.,0.));
#9556=CARTESIAN_POINT('',(0.,0.,0.));
#9557=CARTESIAN_POINT('Origin',(-0.57721779446269,-7.,-9.01236733960726));
#9558=CARTESIAN_POINT('',(-0.57721779446269,-7.,-9.01236733960726));
#9559=CARTESIAN_POINT('',(-0.277898466954226,-7.,-9.50606894332475));
#9560=CARTESIAN_POINT('',(-0.502387962585574,-7.,-9.13579274053664));
#9561=CARTESIAN_POINT('',(-0.277898466954226,-6.6,-9.50606894332475));
#9562=CARTESIAN_POINT('',(-0.277898466954226,-7.,-9.50606894332475));
#9563=CARTESIAN_POINT('',(-0.57721779446269,-6.6,-9.01236733960726));
#9564=CARTESIAN_POINT('',(-0.277898466954226,-6.6,-9.50606894332475));
#9565=CARTESIAN_POINT('',(-0.57721779446269,-7.,-9.01236733960726));
#9566=CARTESIAN_POINT('Origin',(-0.299319327508464,-7.,-8.50629839628252));
#9567=CARTESIAN_POINT('',(-0.299319327508464,-7.,-8.50629839628252));
#9568=CARTESIAN_POINT('',(-0.36879394424702,-7.,-8.6328156321137));
#9569=CARTESIAN_POINT('',(-0.299319327508464,-6.6,-8.50629839628252));
#9570=CARTESIAN_POINT('',(-0.57721779446269,-6.6,-9.01236733960726));
#9571=CARTESIAN_POINT('',(-0.299319327508464,-7.,-8.50629839628252));
#9572=CARTESIAN_POINT('Origin',(0.277898466954227,-7.,-8.49393105667526));
#9573=CARTESIAN_POINT('',(0.277898466954227,-7.,-8.49393105667526));
#9574=CARTESIAN_POINT('',(0.133594018338554,-7.,-8.49702289157707));
#9575=CARTESIAN_POINT('',(0.277898466954227,-6.6,-8.49393105667526));
#9576=CARTESIAN_POINT('',(-0.299319327508464,-6.6,-8.50629839628252));
#9577=CARTESIAN_POINT('',(0.277898466954227,-7.,-8.49393105667526));
#9578=CARTESIAN_POINT('Origin',(0.57721779446269,-7.,-8.98763266039274));
#9579=CARTESIAN_POINT('',(0.57721779446269,-7.,-8.98763266039274));
#9580=CARTESIAN_POINT('',(0.502387962585574,-7.,-8.86420725946337));
#9581=CARTESIAN_POINT('',(0.57721779446269,-6.6,-8.98763266039274));
#9582=CARTESIAN_POINT('',(0.277898466954227,-6.6,-8.49393105667526));
#9583=CARTESIAN_POINT('',(0.57721779446269,-7.,-8.98763266039274));
#9584=CARTESIAN_POINT('Origin',(0.299319327508464,-7.,-9.49370160371748));
#9585=CARTESIAN_POINT('',(0.299319327508464,-7.,-9.49370160371748));
#9586=CARTESIAN_POINT('',(0.36879394424702,-7.,-9.3671843678863));
#9587=CARTESIAN_POINT('',(0.299319327508464,-6.6,-9.49370160371748));
#9588=CARTESIAN_POINT('',(0.57721779446269,-6.6,-8.98763266039274));
#9589=CARTESIAN_POINT('',(0.299319327508464,-7.,-9.49370160371748));
#9590=CARTESIAN_POINT('Origin',(-0.277898466954226,-7.,-9.50606894332475));
#9591=CARTESIAN_POINT('',(-0.133594018338554,-7.,-9.50297710842293));
#9592=CARTESIAN_POINT('',(0.299319327508464,-6.6,-9.49370160371748));
#9593=CARTESIAN_POINT('Origin',(6.93889390390723E-17,-6.6,-9.));
#9594=CARTESIAN_POINT('Origin',(0.,-6.,-9.));
#9595=CARTESIAN_POINT('',(-1.,-6.,-9.));
#9596=CARTESIAN_POINT('Origin',(0.,-6.,-9.));
#9597=CARTESIAN_POINT('',(-1.,-7.,-9.));
#9598=CARTESIAN_POINT('',(-1.,-6.,-9.));
#9599=CARTESIAN_POINT('Origin',(0.,-7.,-9.));
#9600=CARTESIAN_POINT('Origin',(0.,-7.,-9.));
#9601=CARTESIAN_POINT('Origin',(0.,-6.,-9.));
#9806=UNCERTAINTY_MEASURE_WITH_UNIT(LENGTH_MEASURE(0.01),#9823,
'DISTANCE_ACCURACY_VALUE',
'Maximum model space distance between geometric entities at asserted c
onnectivities');
#9811=UNCERTAINTY_MEASURE_WITH_UNIT(LENGTH_MEASURE(0.01),#9823,
'DISTANCE_ACCURACY_VALUE',
'Maximum model space distance between geometric entities at asserted c
onnectivities');
#9817=(
GEOMETRIC_REPRESENTATION_CONTEXT(3)
GLOBAL_UNCERTAINTY_ASSIGNED_CONTEXT((#9806))
GLOBAL_UNIT_ASSIGNED_CONTEXT((#9823,#9825,#9826))
REPRESENTATION_CONTEXT('','3D')
);
#9822=(
GEOMETRIC_REPRESENTATION_CONTEXT(3)
GLOBAL_UNCERTAINTY_ASSIGNED_CONTEXT((#9811))
GLOBAL_UNIT_ASSIGNED_CONTEXT((#9823,#9825,#9826))
REPRESENTATION_CONTEXT('','3D')
);
#9823=(
LENGTH_UNIT()
NAMED_UNIT(*)
SI_UNIT(.MILLI.,.METRE.)
);
#9825=(
NAMED_UNIT(*)
PLANE_ANGLE_UNIT()
SI_UNIT($,.RADIAN.)
);
#9826=(
NAMED_UNIT(*)
SI_UNIT($,.STERADIAN.)
SOLID_ANGLE_UNIT()
);
#9832=SHAPE_DEFINITION_REPRESENTATION(#9842,#9861);
#9842=PRODUCT_DEFINITION_SHAPE('',$,#9872);
#9861=SHAPE_REPRESENTATION('',(#3657),#9817);
#9866=PRODUCT_DEFINITION_CONTEXT('part definition',#9898,'design');
#9872=PRODUCT_DEFINITION('Screw_02','Screw_02',#9882,#9866);
#9882=PRODUCT_DEFINITION_FORMATION('',$,#9905);
#9898=APPLICATION_CONTEXT(
'Core Data for Automotive Mechanical Design Process');
#9899=PRODUCT_CONTEXT('part definition',#9898,'mechanical');
#9905=PRODUCT('Screw_02','Screw_02',$,(#9899));
#9912=PRESENTATION_STYLE_ASSIGNMENT((#9915));
#9915=SURFACE_STYLE_USAGE(.BOTH.,#9918);
#9918=SURFACE_SIDE_STYLE('',(#9921));
#9921=SURFACE_STYLE_FILL_AREA(#9924);
#9924=FILL_AREA_STYLE('Opaque(233,233,233)',(#9927));
#9927=FILL_AREA_STYLE_COLOUR('Opaque(233,233,233)',#9930);
#9930=COLOUR_RGB('Opaque(233,233,233)', 0.40784314, 0.44705882, 0.49803922);
ENDSEC;
END-ISO-10303-21;
